ISO-10303-21;
HEADER;
FILE_DESCRIPTION (('STEP AP214'),
    '1' );
FILE_NAME ('Nut.step',
    '2026-10-28T16:39:03',
    ( '' ),
    ( '' ),
    'SwSTEP 2.0',
    'SolidWorks 2024',
    '' );
FILE_SCHEMA (( 'AUTOMOTIVE_DESIGN' ));
ENDSEC;

DATA;
#11=LINE ( 'NONE', #7275, #2680 ) ;
#14=CARTESIAN_POINT ( 'NONE',  ( -12.99038105676657651, 1.734723475976807094E-15, 0.000000000000000000 ) ) ;
#25=ORIENTED_EDGE ( 'NONE', *, *, #6041, .T. ) ;
#41=DIRECTION ( 'NONE',  ( 0.000000000000000000, -1.000000000000000000, 0.000000000000000000 ) ) ;
#85=EDGE_CURVE ( 'NONE', #4850, #1396, #297, .T. ) ;
#92=CIRCLE ( 'NONE', #7022, 0.5000000000000004441 ) ;
#97=DIRECTION ( 'NONE',  ( 0.5000000000000000000, 0.8660254037844385966, 0.000000000000000000 ) ) ;
#102=FACE_OUTER_BOUND ( 'NONE', #3804, .T. ) ;
#109=VERTEX_POINT ( 'NONE', #3635 ) ;
#110=CARTESIAN_POINT ( 'NONE',  ( -13.00000000000000178, 1.592040838891559293E-15, 7.500000000000000000 ) ) ;
#118=CIRCLE ( 'NONE', #4338, 5.000000000000000888 ) ;
#121=CARTESIAN_POINT ( 'NONE',  ( 10.82531754730547213, 13.75000000000000178, 7.500000000000000000 ) ) ;
#123=DIRECTION ( 'NONE',  ( 1.000000000000000000, 0.000000000000000000, 0.000000000000000000 ) ) ;
#125=CYLINDRICAL_SURFACE ( 'NONE', #7742, 12.50000000000000000 ) ;
#135=ADVANCED_FACE ( 'NONE', ( #1032 ), #5362, .T. ) ;
#137=CARTESIAN_POINT ( 'NONE',  ( 6.495190528383280260, 11.25000000000000000, 7.500000000000000000 ) ) ;
#155=VERTEX_POINT ( 'NONE', #3519 ) ;
#171=DIRECTION ( 'NONE',  ( -0.000000000000000000, 0.000000000000000000, -1.000000000000000000 ) ) ;
#174=DIRECTION ( 'NONE',  ( 0.5000000000000003331, -0.8660254037844383745, 0.000000000000000000 ) ) ;
#181=ORIENTED_EDGE ( 'NONE', *, *, #776, .F. ) ;
#209=CARTESIAN_POINT ( 'NONE',  ( 0.000000000000000000, 0.000000000000000000, 7.500000000000000000 ) ) ;
#216=PLANE ( 'NONE',  #478 ) ;
#265=ORIENTED_EDGE ( 'NONE', *, *, #760, .F. ) ;
#268=VERTEX_POINT ( 'NONE', #6764 ) ;
#271=CARTESIAN_POINT ( 'NONE',  ( 6.495190528383288253, -16.24999999999999645, 7.500000000000000000 ) ) ;
#280=EDGE_LOOP ( 'NONE', ( #6094, #597, #2552, #1101 ) ) ;
#291=EDGE_CURVE ( 'NONE', #4944, #155, #1584, .T. ) ;
#292=ORIENTED_EDGE ( 'NONE', *, *, #6653, .F. ) ;
#297=CIRCLE ( 'NONE', #1708, 5.000000000000000000 ) ;
#300=ORIENTED_EDGE ( 'NONE', *, *, #5315, .T. ) ;
#303=ADVANCED_FACE ( 'NONE', ( #1229 ), #2587, .T. ) ;
#307=AXIS2_PLACEMENT_3D ( 'NONE', #6399, #898, #7680 ) ;
#346=EDGE_CURVE ( 'NONE', #5142, #6431, #1306, .T. ) ;
#360=LINE ( 'NONE', #1436, #2229 ) ;
#364=EDGE_CURVE ( 'NONE', #1519, #5920, #5601, .T. ) ;
#421=FACE_OUTER_BOUND ( 'NONE', #3553, .T. ) ;
#422=CARTESIAN_POINT ( 'NONE',  ( 6.495190528383280260, 11.25000000000000000, 7.500000000000000000 ) ) ;
#436=CARTESIAN_POINT ( 'NONE',  ( 12.99038105676657651, -1.301042606982605321E-15, 7.500000000000000000 ) ) ;
#439=LINE ( 'NONE', #1158, #5506 ) ;
#449=VECTOR ( 'NONE', #4259, 1000.000000000000000 ) ;
#453=( GEOMETRIC_REPRESENTATION_CONTEXT ( 3 ) GLOBAL_UNCERTAINTY_ASSIGNED_CONTEXT ( ( #3202 ) ) GLOBAL_UNIT_ASSIGNED_CONTEXT ( ( #1271, #2470, #555 ) ) REPRESENTATION_CONTEXT ( 'NONE', 'WORKASPACE' ) );
#461=AXIS2_PLACEMENT_3D ( 'NONE', #436, #4234, #5280 ) ;
#474=ORIENTED_EDGE ( 'NONE', *, *, #7618, .F. ) ;
#478=AXIS2_PLACEMENT_3D ( 'NONE', #1977, #2666, #97 ) ;
#490=EDGE_CURVE ( 'NONE', #6450, #7344, #1575, .T. ) ;
#503=AXIS2_PLACEMENT_3D ( 'NONE', #2813, #5247, #2205 ) ;
#504=EDGE_CURVE ( 'NONE', #4687, #756, #6958, .T. ) ;
#510=DIRECTION ( 'NONE',  ( 1.000000000000000000, 0.000000000000000000, 0.000000000000000000 ) ) ;
#521=CARTESIAN_POINT ( 'NONE',  ( -10.82531754730547924, 13.75000000000000000, 7.500000000000000000 ) ) ;
#525=EDGE_CURVE ( 'NONE', #6373, #2940, #4779, .T. ) ;
#537=FACE_OUTER_BOUND ( 'NONE', #7292, .T. ) ;
#539=PRODUCT_DEFINITION_FORMATION_WITH_SPECIFIED_SOURCE ( 'ANY', '', #2574, .NOT_KNOWN. ) ;
#549=APPLICATION_CONTEXT ( 'automotive_design' ) ;
#555=( NAMED_UNIT ( * ) SI_UNIT ( $, .STERADIAN. ) SOLID_ANGLE_UNIT ( ) );
#561=ORIENTED_EDGE ( 'NONE', *, *, #6531, .F. ) ;
#567=EDGE_CURVE ( 'NONE', #3797, #109, #5955, .T. ) ;
#581=CIRCLE ( 'NONE', #307, 13.00000000000000178 ) ;
#597=ORIENTED_EDGE ( 'NONE', *, *, #4395, .T. ) ;
#603=VERTEX_POINT ( 'NONE', #1057 ) ;
#605=DIRECTION ( 'NONE',  ( 0.000000000000000000, 0.000000000000000000, -1.000000000000000000 ) ) ;
#612=CARTESIAN_POINT ( 'NONE',  ( 10.82531754730548279, -13.74999999999999645, 0.000000000000000000 ) ) ;
#618=LINE ( 'NONE', #6112, #1900 ) ;
#622=AXIS2_PLACEMENT_3D ( 'NONE', #1717, #4162, #1598 ) ;
#632=CARTESIAN_POINT ( 'NONE',  ( -6.495190528383287365, 11.25000000000000000, 7.500000000000000000 ) ) ;
#641=LINE ( 'NONE', #3735, #5060 ) ;
#658=DIRECTION ( 'NONE',  ( 0.000000000000000000, -0.000000000000000000, 1.000000000000000000 ) ) ;
#666=EDGE_CURVE ( 'NONE', #5450, #5144, #3150, .T. ) ;
#687=ADVANCED_FACE ( 'NONE', ( #1931, #3034 ), #1818, .T. ) ;
#692=DIRECTION ( 'NONE',  ( -0.000000000000000000, -0.000000000000000000, 1.000000000000000000 ) ) ;
#697=CIRCLE ( 'NONE', #1462, 5.000000000000000000 ) ;
#699=EDGE_LOOP ( 'NONE', ( #2725, #2849, #4765, #6053 ) ) ;
#703=DIRECTION ( 'NONE',  ( 0.000000000000000000, 0.000000000000000000, -1.000000000000000000 ) ) ;
#714=DIRECTION ( 'NONE',  ( -0.5000000000000003331, 0.8660254037844383745, 0.000000000000000000 ) ) ;
#732=PLANE ( 'NONE',  #7801 ) ;
#737=ORIENTED_EDGE ( 'NONE', *, *, #4235, .F. ) ;
#738=ORIENTED_EDGE ( 'NONE', *, *, #787, .T. ) ;
#742=AXIS2_PLACEMENT_3D ( 'NONE', #2433, #7878, #7098 ) ;
#750=CYLINDRICAL_SURFACE ( 'NONE', #3535, 12.50000000000000000 ) ;
#756=VERTEX_POINT ( 'NONE', #7471 ) ;
#760=EDGE_CURVE ( 'NONE', #2724, #6891, #6193, .T. ) ;
#776=EDGE_CURVE ( 'NONE', #6431, #2724, #3901, .T. ) ;
#777=CARTESIAN_POINT ( 'NONE',  ( 18.76388374866283471, -1.044563157018773529E-16, 7.500000000000000000 ) ) ;
#787=EDGE_CURVE ( 'NONE', #756, #6450, #697, .T. ) ;
#789=ORIENTED_EDGE ( 'NONE', *, *, #7829, .F. ) ;
#794=ORIENTED_EDGE ( 'NONE', *, *, #567, .F. ) ;
#803=EDGE_CURVE ( 'NONE', #3524, #2004, #5949, .T. ) ;
#811=ORIENTED_EDGE ( 'NONE', *, *, #6848, .F. ) ;
#867=ORIENTED_EDGE ( 'NONE', *, *, #3488, .F. ) ;
#898=DIRECTION ( 'NONE',  ( 0.000000000000000000, -0.000000000000000000, 1.000000000000000000 ) ) ;
#899=EDGE_LOOP ( 'NONE', ( #6972, #5043, #1433, #7453 ) ) ;
#904=DIRECTION ( 'NONE',  ( 1.000000000000000000, 0.000000000000000000, 0.000000000000000000 ) ) ;
#923=DIRECTION ( 'NONE',  ( -1.000000000000000000, 0.000000000000000000, 0.000000000000000000 ) ) ;
#952=ORIENTED_EDGE ( 'NONE', *, *, #2825, .T. ) ;
#960=EDGE_CURVE ( 'NONE', #6891, #5142, #965, .T. ) ;
#963=AXIS2_PLACEMENT_3D ( 'NONE', #1645, #605, #1119 ) ;
#965=CIRCLE ( 'NONE', #5831, 5.000000000000000000 ) ;
#977=ORIENTED_EDGE ( 'NONE', *, *, #6848, .T. ) ;
#980=EDGE_CURVE ( 'NONE', #2150, #3842, #7114, .T. ) ;
#996=EDGE_LOOP ( 'NONE', ( #6726, #6202, #7641, #4101 ) ) ;
#998=LINE ( 'NONE', #4122, #3408 ) ;
#1005=CARTESIAN_POINT ( 'NONE',  ( -17.32050807568877104, -2.499999999999999112, 7.500000000000000000 ) ) ;
#1011=EDGE_CURVE ( 'NONE', #7344, #4687, #5447, .T. ) ;
#1020=VECTOR ( 'NONE', #3603, 1000.000000000000000 ) ;
#1032=FACE_OUTER_BOUND ( 'NONE', #899, .T. ) ;
#1041=ORIENTED_EDGE ( 'NONE', *, *, #364, .F. ) ;
#1051=DIRECTION ( 'NONE',  ( 0.5000000000000000000, 0.8660254037844385966, 0.000000000000000000 ) ) ;
#1057=CARTESIAN_POINT ( 'NONE',  ( 12.50000000000000000, 1.530808498934191521E-15, 0.5000000000000004441 ) ) ;
#1075=VECTOR ( 'NONE', #6397, 1000.000000000000000 ) ;
#1093=CIRCLE ( 'NONE', #461, 5.000000000000000888 ) ;
#1097=CARTESIAN_POINT ( 'NONE',  ( 6.495190528383280260, 16.25000000000000000, 7.500000000000000000 ) ) ;
#1101=ORIENTED_EDGE ( 'NONE', *, *, #504, .T. ) ;
#1112=EDGE_LOOP ( 'NONE', ( #811, #5926, #6831, #2872 ) ) ;
#1119=DIRECTION ( 'NONE',  ( -1.000000000000000000, 0.000000000000000000, 0.000000000000000000 ) ) ;
#1158=CARTESIAN_POINT ( 'NONE',  ( -17.32050807568877104, 2.500000000000002220, 7.500000000000000000 ) ) ;
#1206=VECTOR ( 'NONE', #4255, 1000.000000000000114 ) ;
#1214=DIRECTION ( 'NONE',  ( 0.000000000000000000, -0.000000000000000000, 1.000000000000000000 ) ) ;
#1229=FACE_OUTER_BOUND ( 'NONE', #1450, .T. ) ;
#1230=DIRECTION ( 'NONE',  ( 0.8660254037844384856, 0.5000000000000003331, -0.000000000000000000 ) ) ;
#1255=DIRECTION ( 'NONE',  ( 1.000000000000000000, 0.000000000000000000, 0.000000000000000000 ) ) ;
#1271=( LENGTH_UNIT ( ) NAMED_UNIT ( * ) SI_UNIT ( .MILLI., .METRE. ) );
#1274=CIRCLE ( 'NONE', #5757, 5.000000000000000888 ) ;
#1275=ORIENTED_EDGE ( 'NONE', *, *, #1932, .T. ) ;
#1289=DIRECTION ( 'NONE',  ( 0.000000000000000000, -0.000000000000000000, 1.000000000000000000 ) ) ;
#1293=( GEOMETRIC_REPRESENTATION_CONTEXT ( 3 ) GLOBAL_UNCERTAINTY_ASSIGNED_CONTEXT ( ( #6402 ) ) GLOBAL_UNIT_ASSIGNED_CONTEXT ( ( #2786, #5675, #4615 ) ) REPRESENTATION_CONTEXT ( 'NONE', 'WORKASPACE' ) );
#1306=LINE ( 'NONE', #6200, #6968 ) ;
#1311=EDGE_CURVE ( 'NONE', #7344, #2724, #6336, .T. ) ;
#1334=AXIS2_PLACEMENT_3D ( 'NONE', #5899, #3637, #6500 ) ;
#1335=AXIS2_PLACEMENT_3D ( 'NONE', #14, #5547, #7319 ) ;
#1361=CARTESIAN_POINT ( 'NONE',  ( 0.000000000000000000, 0.000000000000000000, 0.5000000000000004441 ) ) ;
#1365=FACE_OUTER_BOUND ( 'NONE', #3266, .T. ) ;
#1374=EDGE_CURVE ( 'NONE', #2940, #4850, #360, .T. ) ;
#1389=DIRECTION ( 'NONE',  ( -1.000000000000000000, 0.000000000000000000, 0.000000000000000000 ) ) ;
#1393=AXIS2_PLACEMENT_3D ( 'NONE', #5095, #7550, #3299 ) ;
#1396=VERTEX_POINT ( 'NONE', #2691 ) ;
#1406=ORIENTED_EDGE ( 'NONE', *, *, #7332, .T. ) ;
#1407=PLANE ( 'NONE',  #4149 ) ;
#1423=ORIENTED_EDGE ( 'NONE', *, *, #666, .F. ) ;
#1433=ORIENTED_EDGE ( 'NONE', *, *, #1011, .F. ) ;
#1435=DIRECTION ( 'NONE',  ( -1.000000000000000000, 1.224646799147353454E-16, 0.000000000000000000 ) ) ;
#1436=CARTESIAN_POINT ( 'NONE',  ( -6.495190528383286477, 16.25000000000000000, 7.500000000000000000 ) ) ;
#1441=ADVANCED_FACE ( 'NONE', ( #7880, #1641 ), #6164, .F. ) ;
#1450=EDGE_LOOP ( 'NONE', ( #5658, #6096, #3235, #1646 ) ) ;
#1462=AXIS2_PLACEMENT_3D ( 'NONE', #3077, #5511, #7908 ) ;
#1475=MANIFOLD_SOLID_BREP ( 'Radyus2', #6708 ) ;
#1480=CARTESIAN_POINT ( 'NONE',  ( -13.00000000000000178, 1.592040838891559293E-15, 6.999999999999999112 ) ) ;
#1492=ADVANCED_FACE ( 'NONE', ( #7328 ), #1824, .F. ) ;
#1508=VECTOR ( 'NONE', #3531, 1000.000000000000000 ) ;
#1517=ORIENTED_EDGE ( 'NONE', *, *, #291, .T. ) ;
#1519=VERTEX_POINT ( 'NONE', #7561 ) ;
#1560=DIRECTION ( 'NONE',  ( 1.000000000000000000, 0.000000000000000000, 0.000000000000000000 ) ) ;
#1564=ADVANCED_FACE ( 'NONE', ( #102 ), #5680, .T. ) ;
#1575=LINE ( 'NONE', #3949, #4277 ) ;
#1584=CIRCLE ( 'NONE', #4015, 13.00000000000000178 ) ;
#1598=DIRECTION ( 'NONE',  ( 1.000000000000000000, 0.000000000000000000, 0.000000000000000000 ) ) ;
#1620=VERTEX_POINT ( 'NONE', #6201 ) ;
#1641=FACE_OUTER_BOUND ( 'NONE', #3480, .T. ) ;
#1645=CARTESIAN_POINT ( 'NONE',  ( -12.99038105676657651, 1.734723475976807094E-15, 7.500000000000000000 ) ) ;
#1646=ORIENTED_EDGE ( 'NONE', *, *, #7671, .F. ) ;
#1708=AXIS2_PLACEMENT_3D ( 'NONE', #1750, #7290, #7212 ) ;
#1717=CARTESIAN_POINT ( 'NONE',  ( 12.99038105676657651, -1.301042606982605321E-15, 0.000000000000000000 ) ) ;
#1724=AXIS2_PLACEMENT_3D ( 'NONE', #209, #6989, #2658 ) ;
#1728=EDGE_CURVE ( 'NONE', #155, #4944, #581, .T. ) ;
#1747=EDGE_CURVE ( 'NONE', #1519, #3303, #2106, .T. ) ;
#1750=CARTESIAN_POINT ( 'NONE',  ( -6.495190528383287365, 11.25000000000000000, 7.500000000000000000 ) ) ;
#1770=DIRECTION ( 'NONE',  ( -0.8660254037844387076, 0.5000000000000001110, 0.000000000000000000 ) ) ;
#1789=DIRECTION ( 'NONE',  ( -0.000000000000000000, 0.000000000000000000, -1.000000000000000000 ) ) ;
#1818=PLANE ( 'NONE',  #6211 ) ;
#1824=PLANE ( 'NONE',  #7489 ) ;
#1866=CARTESIAN_POINT ( 'NONE',  ( 12.50000000000000000, 1.530808498934191521E-15, 6.999999999999999112 ) ) ;
#1878=ORIENTED_EDGE ( 'NONE', *, *, #980, .T. ) ;
#1900=VECTOR ( 'NONE', #4296, 1000.000000000000114 ) ;
#1926=DIRECTION ( 'NONE',  ( -0.000000000000000000, -0.000000000000000000, -1.000000000000000000 ) ) ;
#1931=FACE_BOUND ( 'NONE', #6605, .T. ) ;
#1932=EDGE_CURVE ( 'NONE', #5833, #4850, #6308, .T. ) ;
#1933=ADVANCED_FACE ( 'NONE', ( #3151 ), #7474, .T. ) ;
#1963=AXIS2_PLACEMENT_3D ( 'NONE', #7195, #5505, #5988 ) ;
#1968=CARTESIAN_POINT ( 'NONE',  ( 6.495190528383288253, -16.24999999999999645, 7.500000000000000000 ) ) ;
#1973=DIRECTION ( 'NONE',  ( 1.000000000000000000, 0.000000000000000000, 0.000000000000000000 ) ) ;
#1977=CARTESIAN_POINT ( 'NONE',  ( -9.381941874331415576, 16.25000000000000000, 7.500000000000000000 ) ) ;
#1996=ORIENTED_EDGE ( 'NONE', *, *, #1747, .T. ) ;
#2004=VERTEX_POINT ( 'NONE', #7438 ) ;
#2006=VECTOR ( 'NONE', #4742, 1000.000000000000000 ) ;
#2018=ORIENTED_EDGE ( 'NONE', *, *, #346, .F. ) ;
#2058=FACE_OUTER_BOUND ( 'NONE', #1112, .T. ) ;
#2067=ORIENTED_EDGE ( 'NONE', *, *, #3718, .F. ) ;
#2089=CARTESIAN_POINT ( 'NONE',  ( 6.495190528383289141, -11.24999999999999645, 7.500000000000000000 ) ) ;
#2106=CIRCLE ( 'NONE', #3658, 12.50000000000000000 ) ;
#2130=AXIS2_PLACEMENT_3D ( 'NONE', #5914, #6474, #6997 ) ;
#2150=VERTEX_POINT ( 'NONE', #2175 ) ;
#2167=CARTESIAN_POINT ( 'NONE',  ( -10.82531754730547924, 13.75000000000000000, 0.000000000000000000 ) ) ;
#2172=DIRECTION ( 'NONE',  ( 0.000000000000000000, -1.000000000000000000, -0.000000000000000000 ) ) ;
#2175=CARTESIAN_POINT ( 'NONE',  ( 13.00000000000000178, 0.000000000000000000, 7.500000000000000000 ) ) ;
#2205=DIRECTION ( 'NONE',  ( 1.000000000000000000, 0.000000000000000000, 0.000000000000000000 ) ) ;
#2229=VECTOR ( 'NONE', #5086, 1000.000000000000000 ) ;
#2231=PRODUCT_DEFINITION ( 'UNKNOWN', '', #539, #7599 ) ;
#2242=EDGE_CURVE ( 'NONE', #5920, #4944, #3890, .T. ) ;
#2243=ADVANCED_FACE ( 'NONE', ( #537 ), #2457, .F. ) ;
#2250=ORIENTED_EDGE ( 'NONE', *, *, #2297, .F. ) ;
#2258=ORIENTED_EDGE ( 'NONE', *, *, #5071, .F. ) ;
#2266=DIRECTION ( 'NONE',  ( 0.000000000000000000, 0.000000000000000000, -1.000000000000000000 ) ) ;
#2271=LINE ( 'NONE', #4699, #7540 ) ;
#2274=ORIENTED_EDGE ( 'NONE', *, *, #7240, .T. ) ;
#2291=ORIENTED_EDGE ( 'NONE', *, *, #7091, .T. ) ;
#2297=EDGE_CURVE ( 'NONE', #3524, #4687, #4216, .T. ) ;
#2311=CARTESIAN_POINT ( 'NONE',  ( -17.32050807568877104, -2.499999999999999556, 7.500000000000000000 ) ) ;
#2312=DIRECTION ( 'NONE',  ( 0.000000000000000000, 0.000000000000000000, -1.000000000000000000 ) ) ;
#2317=ORIENTED_EDGE ( 'NONE', *, *, #6348, .T. ) ;
#2328=LINE ( 'NONE', #4762, #1508 ) ;
#2335=CARTESIAN_POINT ( 'NONE',  ( -6.495190528383286477, 16.25000000000000000, 7.500000000000000000 ) ) ;
#2345=DIRECTION ( 'NONE',  ( -1.000000000000000000, 0.000000000000000000, 0.000000000000000000 ) ) ;
#2351=DIRECTION ( 'NONE',  ( 1.000000000000000000, 0.000000000000000000, 0.000000000000000000 ) ) ;
#2361=ORIENTED_EDGE ( 'NONE', *, *, #980, .F. ) ;
#2362=VECTOR ( 'NONE', #7716, 1000.000000000000000 ) ;
#2389=ADVANCED_FACE ( 'NONE', ( #2653 ), #1407, .F. ) ;
#2401=LINE ( 'NONE', #521, #1020 ) ;
#2403=DIRECTION ( 'NONE',  ( 0.000000000000000000, 0.000000000000000000, -1.000000000000000000 ) ) ;
#2420=CARTESIAN_POINT ( 'NONE',  ( -6.495190528383282036, -16.24999999999999645, 0.000000000000000000 ) ) ;
#2433=CARTESIAN_POINT ( 'NONE',  ( 6.495190528383289141, -11.24999999999999645, 7.500000000000000000 ) ) ;
#2457=PLANE ( 'NONE',  #3771 ) ;
#2460=DIRECTION ( 'NONE',  ( -0.5000000000000000000, -0.8660254037844385966, 0.000000000000000000 ) ) ;
#2462=DIRECTION ( 'NONE',  ( 0.000000000000000000, 1.000000000000000000, 0.000000000000000000 ) ) ;
#2470=( NAMED_UNIT ( * ) PLANE_ANGLE_UNIT ( ) SI_UNIT ( $, .RADIAN. ) );
#2471=ORIENTED_EDGE ( 'NONE', *, *, #7535, .T. ) ;
#2474=ADVANCED_FACE ( 'NONE', ( #1365 ), #125, .F. ) ;
#2508=DIRECTION ( 'NONE',  ( -0.8660254037844384856, -0.5000000000000004441, 0.000000000000000000 ) ) ;
#2517=VERTEX_POINT ( 'NONE', #1005 ) ;
#2546=AXIS2_PLACEMENT_3D ( 'NONE', #422, #2312, #2345 ) ;
#2552=ORIENTED_EDGE ( 'NONE', *, *, #2297, .T. ) ;
#2574=PRODUCT ( 'Nut', 'Nut', '', ( #5387 ) ) ;
#2577=FACE_OUTER_BOUND ( 'NONE', #5442, .T. ) ;
#2578=CARTESIAN_POINT ( 'NONE',  ( 0.000000000000000000, 0.000000000000000000, 7.500000000000000000 ) ) ;
#2586=CARTESIAN_POINT ( 'NONE',  ( 10.82531754730547213, 13.75000000000000178, 0.000000000000000000 ) ) ;
#2587=CYLINDRICAL_SURFACE ( 'NONE', #7104, 5.000000000000000000 ) ;
#2629=DIRECTION ( 'NONE',  ( 0.000000000000000000, 0.000000000000000000, -1.000000000000000000 ) ) ;
#2646=ORIENTED_EDGE ( 'NONE', *, *, #291, .F. ) ;
#2648=DIRECTION ( 'NONE',  ( 0.000000000000000000, -0.000000000000000000, 1.000000000000000000 ) ) ;
#2653=FACE_OUTER_BOUND ( 'NONE', #3966, .T. ) ;
#2658=DIRECTION ( 'NONE',  ( 1.000000000000000000, 0.000000000000000000, 0.000000000000000000 ) ) ;
#2666=DIRECTION ( 'NONE',  ( 0.8660254037844387076, -0.5000000000000001110, 0.000000000000000000 ) ) ;
#2669=DIRECTION ( 'NONE',  ( -0.000000000000000000, 0.000000000000000000, -1.000000000000000000 ) ) ;
#2680=VECTOR ( 'NONE', #2460, 1000.000000000000227 ) ;
#2691=CARTESIAN_POINT ( 'NONE',  ( -10.82531754730547924, 13.75000000000000000, 7.500000000000000000 ) ) ;
#2719=LINE ( 'NONE', #7456, #7654 ) ;
#2724=VERTEX_POINT ( 'NONE', #5455 ) ;
#2725=ORIENTED_EDGE ( 'NONE', *, *, #7391, .F. ) ;
#2726=CARTESIAN_POINT ( 'NONE',  ( 10.82531754730548279, -13.74999999999999645, 7.500000000000000000 ) ) ;
#2745=CARTESIAN_POINT ( 'NONE',  ( 18.76388374866283471, -1.044563157018773529E-16, 0.000000000000000000 ) ) ;
#2749=ADVANCED_FACE ( 'NONE', ( #7222 ), #6694, .T. ) ;
#2786=( LENGTH_UNIT ( ) NAMED_UNIT ( * ) SI_UNIT ( .MILLI., .METRE. ) );
#2803=CIRCLE ( 'NONE', #6380, 5.000000000000000000 ) ;
#2813=CARTESIAN_POINT ( 'NONE',  ( 0.000000000000000000, 0.000000000000000000, 7.500000000000000000 ) ) ;
#2825=EDGE_CURVE ( 'NONE', #603, #5920, #5705, .T. ) ;
#2831=DIRECTION ( 'NONE',  ( -1.000000000000000000, 0.000000000000000000, 0.000000000000000000 ) ) ;
#2849=ORIENTED_EDGE ( 'NONE', *, *, #3726, .T. ) ;
#2872=ORIENTED_EDGE ( 'NONE', *, *, #666, .T. ) ;
#2875=ORIENTED_EDGE ( 'NONE', *, *, #2825, .F. ) ;
#2940=VERTEX_POINT ( 'NONE', #3770 ) ;
#2941=VECTOR ( 'NONE', #6517, 1000.000000000000227 ) ;
#2944=CARTESIAN_POINT ( 'NONE',  ( -6.495190528383287365, 11.25000000000000000, 0.000000000000000000 ) ) ;
#2954=LINE ( 'NONE', #2311, #2006 ) ;
#2965=CARTESIAN_POINT ( 'NONE',  ( -6.495190528383282036, -11.24999999999999645, 7.500000000000000000 ) ) ;
#3010=ORIENTED_EDGE ( 'NONE', *, *, #6531, .T. ) ;
#3034=FACE_OUTER_BOUND ( 'NONE', #3592, .T. ) ;
#3077=CARTESIAN_POINT ( 'NONE',  ( -6.495190528383282036, -11.24999999999999645, 7.500000000000000000 ) ) ;
#3086=DIRECTION ( 'NONE',  ( -1.000000000000000000, 0.000000000000000000, 0.000000000000000000 ) ) ;
#3112=CARTESIAN_POINT ( 'NONE',  ( 9.381941874331406694, 16.25000000000000000, 7.500000000000000000 ) ) ;
#3134=VECTOR ( 'NONE', #5762, 1000.000000000000000 ) ;
#3150=LINE ( 'NONE', #5636, #7612 ) ;
#3151=FACE_OUTER_BOUND ( 'NONE', #4965, .T. ) ;
#3157=DIRECTION ( 'NONE',  ( 0.000000000000000000, 0.000000000000000000, -1.000000000000000000 ) ) ;
#3171=EDGE_CURVE ( 'NONE', #1620, #3797, #1093, .T. ) ;
#3202=UNCERTAINTY_MEASURE_WITH_UNIT (LENGTH_MEASURE( 1.000000000000000082E-05 ), #1271, 'distance_accuracy_value', 'NONE');
#3230=PLANE ( 'NONE',  #4813 ) ;
#3235=ORIENTED_EDGE ( 'NONE', *, *, #4828, .F. ) ;
#3244=CARTESIAN_POINT ( 'NONE',  ( -12.99038105676657651, 1.734723475976807094E-15, 7.500000000000000000 ) ) ;
#3256=FACE_OUTER_BOUND ( 'NONE', #6811, .T. ) ;
#3266=EDGE_LOOP ( 'NONE', ( #561, #6662, #6903, #4512 ) ) ;
#3276=ORIENTED_EDGE ( 'NONE', *, *, #4634, .T. ) ;
#3298=CYLINDRICAL_SURFACE ( 'NONE', #4566, 5.000000000000000888 ) ;
#3299=DIRECTION ( 'NONE',  ( 1.000000000000000000, 0.000000000000000000, 0.000000000000000000 ) ) ;
#3303=VERTEX_POINT ( 'NONE', #1866 ) ;
#3310=CARTESIAN_POINT ( 'NONE',  ( -10.82531754730547568, -13.74999999999999822, 7.500000000000000000 ) ) ;
#3335=LINE ( 'NONE', #3887, #7156 ) ;
#3364=LINE ( 'NONE', #7573, #4207 ) ;
#3370=DIRECTION ( 'NONE',  ( -0.000000000000000000, -0.000000000000000000, -1.000000000000000000 ) ) ;
#3394=ORIENTED_EDGE ( 'NONE', *, *, #1728, .T. ) ;
#3396=CARTESIAN_POINT ( 'NONE',  ( 0.000000000000000000, 0.000000000000000000, 0.5000000000000004441 ) ) ;
#3408=VECTOR ( 'NONE', #6574, 1000.000000000000000 ) ;
#3426=CARTESIAN_POINT ( 'NONE',  ( 9.381941874331417353, -16.24999999999999645, 0.000000000000000000 ) ) ;
#3435=ORIENTED_EDGE ( 'NONE', *, *, #7115, .T. ) ;
#3460=CIRCLE ( 'NONE', #5523, 12.50000000000000000 ) ;
#3478=VERTEX_POINT ( 'NONE', #4694 ) ;
#3480=EDGE_LOOP ( 'NONE', ( #2250, #4398, #25, #7064, #5731, #7426, #3435, #6441, #7746, #4344, #7223, #7363, #4468 ) ) ;
#3483=DIRECTION ( 'NONE',  ( -1.000000000000000000, 0.000000000000000000, 0.000000000000000000 ) ) ;
#3488=EDGE_CURVE ( 'NONE', #5142, #1620, #6429, .T. ) ;
#3519=CARTESIAN_POINT ( 'NONE',  ( 13.00000000000000178, 0.000000000000000000, 2.168404344971008868E-16 ) ) ;
#3524=VERTEX_POINT ( 'NONE', #5385 ) ;
#3531=DIRECTION ( 'NONE',  ( -0.000000000000000000, -0.000000000000000000, 1.000000000000000000 ) ) ;
#3535=AXIS2_PLACEMENT_3D ( 'NONE', #6247, #4473, #1389 ) ;
#3544=LINE ( 'NONE', #3426, #2941 ) ;
#3553=EDGE_LOOP ( 'NONE', ( #4559, #2875, #3276, #2646 ) ) ;
#3576=TOROIDAL_SURFACE ( 'NONE', #1393, 13.00000000000000178, 0.5000000000000000000 ) ;
#3592=EDGE_LOOP ( 'NONE', ( #6539, #2317, #6143, #1406, #738, #3772, #7856, #6876, #7477, #977, #2291, #1275, #7536 ) ) ;
#3597=CYLINDRICAL_SURFACE ( 'NONE', #742, 5.000000000000000000 ) ;
#3600=ORIENTED_EDGE ( 'NONE', *, *, #7291, .F. ) ;
#3603=DIRECTION ( 'NONE',  ( 0.000000000000000000, 0.000000000000000000, -1.000000000000000000 ) ) ;
#3619=CARTESIAN_POINT ( 'NONE',  ( -12.99038105676657651, 1.734723475976807094E-15, 7.500000000000000000 ) ) ;
#3635=CARTESIAN_POINT ( 'NONE',  ( 17.32050807568877104, 2.500000000000000444, 0.000000000000000000 ) ) ;
#3637=DIRECTION ( 'NONE',  ( 0.000000000000000000, -0.000000000000000000, 1.000000000000000000 ) ) ;
#3658=AXIS2_PLACEMENT_3D ( 'NONE', #7803, #658, #510 ) ;
#3673=DIRECTION ( 'NONE',  ( 0.000000000000000000, -0.000000000000000000, 1.000000000000000000 ) ) ;
#3683=DIRECTION ( 'NONE',  ( -0.5000000000000003331, 0.8660254037844384856, 0.000000000000000000 ) ) ;
#3718=EDGE_CURVE ( 'NONE', #6450, #6891, #998, .T. ) ;
#3726=EDGE_CURVE ( 'NONE', #3478, #2004, #641, .T. ) ;
#3735=CARTESIAN_POINT ( 'NONE',  ( -17.99038105676657651, 1.734723475976807094E-15, 7.500000000000000000 ) ) ;
#3753=DIRECTION ( 'NONE',  ( 1.000000000000000000, 0.000000000000000000, 0.000000000000000000 ) ) ;
#3759=CARTESIAN_POINT ( 'NONE',  ( 0.000000000000000000, 0.000000000000000000, 0.000000000000000000 ) ) ;
#3770=CARTESIAN_POINT ( 'NONE',  ( -6.495190528383286477, 16.25000000000000000, 0.000000000000000000 ) ) ;
#3771=AXIS2_PLACEMENT_3D ( 'NONE', #4891, #1770, #7313 ) ;
#3772=ORIENTED_EDGE ( 'NONE', *, *, #3718, .T. ) ;
#3793=CARTESIAN_POINT ( 'NONE',  ( 0.000000000000000000, 0.000000000000000000, 6.999999999999999112 ) ) ;
#3797=VERTEX_POINT ( 'NONE', #6212 ) ;
#3803=FACE_OUTER_BOUND ( 'NONE', #4210, .T. ) ;
#3804=EDGE_LOOP ( 'NONE', ( #7338, #292, #6255, #794 ) ) ;
#3828=CIRCLE ( 'NONE', #5228, 0.5000000000000004441 ) ;
#3842=VERTEX_POINT ( 'NONE', #110 ) ;
#3849=ADVANCED_FACE ( 'NONE', ( #3803 ), #750, .F. ) ;
#3887=CARTESIAN_POINT ( 'NONE',  ( 12.50000000000000000, 1.530808498934191521E-15, 7.500000000000000000 ) ) ;
#3890=CIRCLE ( 'NONE', #1963, 0.5000000000000004441 ) ;
#3901=CIRCLE ( 'NONE', #6086, 5.000000000000000000 ) ;
#3949=CARTESIAN_POINT ( 'NONE',  ( -6.495190528383282036, -16.24999999999999645, 7.500000000000000000 ) ) ;
#3966=EDGE_LOOP ( 'NONE', ( #7520, #2471, #6573, #7425 ) ) ;
#3973=DIRECTION ( 'NONE',  ( 0.000000000000000000, 0.000000000000000000, -1.000000000000000000 ) ) ;
#3989=DIRECTION ( 'NONE',  ( -0.000000000000000000, 0.000000000000000000, -1.000000000000000000 ) ) ;
#4000=ORIENTED_EDGE ( 'NONE', *, *, #6041, .F. ) ;
#4015=AXIS2_PLACEMENT_3D ( 'NONE', #3759, #5554, #7408 ) ;
#4071=CIRCLE ( 'NONE', #622, 5.000000000000000888 ) ;
#4101=ORIENTED_EDGE ( 'NONE', *, *, #7671, .T. ) ;
#4110=CARTESIAN_POINT ( 'NONE',  ( 0.000000000000000000, 0.000000000000000000, 0.000000000000000000 ) ) ;
#4122=CARTESIAN_POINT ( 'NONE',  ( -9.381941874331412023, -16.24999999999999645, 7.500000000000000000 ) ) ;
#4149=AXIS2_PLACEMENT_3D ( 'NONE', #6909, #41, #7506 ) ;
#4162=DIRECTION ( 'NONE',  ( -0.000000000000000000, 0.000000000000000000, -1.000000000000000000 ) ) ;
#4171=DIRECTION ( 'NONE',  ( -0.000000000000000000, 0.000000000000000000, -1.000000000000000000 ) ) ;
#4182=ORIENTED_EDGE ( 'NONE', *, *, #5071, .T. ) ;
#4185=ADVANCED_FACE ( 'NONE', ( #2058 ), #3230, .F. ) ;
#4186=DIRECTION ( 'NONE',  ( 0.000000000000000000, 0.000000000000000000, 1.000000000000000000 ) ) ;
#4207=VECTOR ( 'NONE', #5777, 1000.000000000000000 ) ;
#4210=EDGE_LOOP ( 'NONE', ( #1996, #3010, #952, #1041 ) ) ;
#4216=LINE ( 'NONE', #7830, #1206 ) ;
#4234=DIRECTION ( 'NONE',  ( 0.000000000000000000, -0.000000000000000000, 1.000000000000000000 ) ) ;
#4235=EDGE_CURVE ( 'NONE', #3303, #1519, #5467, .T. ) ;
#4243=ADVANCED_FACE ( 'NONE', ( #6921 ), #216, .F. ) ;
#4255=DIRECTION ( 'NONE',  ( 0.5000000000000003331, -0.8660254037844384856, 0.000000000000000000 ) ) ;
#4259=DIRECTION ( 'NONE',  ( -0.000000000000000000, -0.000000000000000000, 1.000000000000000000 ) ) ;
#4267=CARTESIAN_POINT ( 'NONE',  ( -18.76388374866283471, 7.854341805648601650E-17, 7.500000000000000000 ) ) ;
#4276=VERTEX_POINT ( 'NONE', #4657 ) ;
#4277=VECTOR ( 'NONE', #2669, 1000.000000000000000 ) ;
#4281=DIRECTION ( 'NONE',  ( -0.000000000000000000, 0.000000000000000000, -1.000000000000000000 ) ) ;
#4283=STYLED_ITEM('',(#7969),#1475);
#4296=DIRECTION ( 'NONE',  ( 0.5000000000000003331, -0.8660254037844384856, 0.000000000000000000 ) ) ;
#4305=ORIENTED_EDGE ( 'NONE', *, *, #6653, .T. ) ;
#4312=TOROIDAL_SURFACE ( 'NONE', #2130, 13.00000000000000178, 0.5000000000000000000 ) ;
#4331=EDGE_CURVE ( 'NONE', #109, #5450, #7632, .T. ) ;
#4338=AXIS2_PLACEMENT_3D ( 'NONE', #3619, #1289, #123 ) ;
#4342=ADVANCED_FACE ( 'NONE', ( #421 ), #4312, .T. ) ;
#4344=ORIENTED_EDGE ( 'NONE', *, *, #7240, .F. ) ;
#4395=EDGE_CURVE ( 'NONE', #2517, #3524, #2954, .T. ) ;
#4398=ORIENTED_EDGE ( 'NONE', *, *, #803, .T. ) ;
#4437=AXIS2_PLACEMENT_3D ( 'NONE', #4495, #2172, #5904 ) ;
#4468=ORIENTED_EDGE ( 'NONE', *, *, #1011, .T. ) ;
#4473=DIRECTION ( 'NONE',  ( -0.000000000000000000, -0.000000000000000000, -1.000000000000000000 ) ) ;
#4488=ORIENTED_EDGE ( 'NONE', *, *, #1311, .T. ) ;
#4495=CARTESIAN_POINT ( 'NONE',  ( 13.00000000000000178, 0.000000000000000000, 0.5000000000000004441 ) ) ;
#4496=DIRECTION ( 'NONE',  ( 1.000000000000000000, 0.000000000000000000, 0.000000000000000000 ) ) ;
#4512=ORIENTED_EDGE ( 'NONE', *, *, #7829, .T. ) ;
#4521=AXIS2_PLACEMENT_3D ( 'NONE', #2965, #1789, #3483 ) ;
#4536=DIRECTION ( 'NONE',  ( 0.000000000000000000, -0.000000000000000000, 1.000000000000000000 ) ) ;
#4559=ORIENTED_EDGE ( 'NONE', *, *, #2242, .F. ) ;
#4563=FACE_OUTER_BOUND ( 'NONE', #6492, .T. ) ;
#4566=AXIS2_PLACEMENT_3D ( 'NONE', #7585, #3973, #923 ) ;
#4605=CARTESIAN_POINT ( 'NONE',  ( -9.381941874331412023, -16.24999999999999645, 0.000000000000000000 ) ) ;
#4615=( NAMED_UNIT ( * ) SI_UNIT ( $, .STERADIAN. ) SOLID_ANGLE_UNIT ( ) );
#4634=EDGE_CURVE ( 'NONE', #603, #155, #7521, .T. ) ;
#4640=FACE_OUTER_BOUND ( 'NONE', #7771, .T. ) ;
#4657=CARTESIAN_POINT ( 'NONE',  ( 17.32050807568877104, -2.500000000000002220, 0.000000000000000000 ) ) ;
#4687=VERTEX_POINT ( 'NONE', #7622 ) ;
#4694=CARTESIAN_POINT ( 'NONE',  ( -17.99038105676657651, 1.734723475976807094E-15, 7.500000000000000000 ) ) ;
#4699=CARTESIAN_POINT ( 'NONE',  ( -9.381941874331415576, 16.25000000000000000, 7.500000000000000000 ) ) ;
#4725=ADVANCED_FACE ( 'NONE', ( #6425 ), #3298, .T. ) ;
#4742=DIRECTION ( 'NONE',  ( 0.000000000000000000, 0.000000000000000000, -1.000000000000000000 ) ) ;
#4762=CARTESIAN_POINT ( 'NONE',  ( 17.32050807568877104, -2.500000000000002220, 7.500000000000000000 ) ) ;
#4765=ORIENTED_EDGE ( 'NONE', *, *, #803, .F. ) ;
#4779=LINE ( 'NONE', #7869, #7606 ) ;
#4794=VECTOR ( 'NONE', #7552, 1000.000000000000000 ) ;
#4813=AXIS2_PLACEMENT_3D ( 'NONE', #777, #2508, #174 ) ;
#4828=EDGE_CURVE ( 'NONE', #6609, #2940, #7899, .T. ) ;
#4843=CIRCLE ( 'NONE', #7161, 5.000000000000000000 ) ;
#4850=VERTEX_POINT ( 'NONE', #2335 ) ;
#4891=CARTESIAN_POINT ( 'NONE',  ( 9.381941874331417353, -16.24999999999999645, 7.500000000000000000 ) ) ;
#4898=DIRECTION ( 'NONE',  ( 0.000000000000000000, -0.000000000000000000, 1.000000000000000000 ) ) ;
#4922=DIRECTION ( 'NONE',  ( 1.000000000000000000, 0.000000000000000000, 0.000000000000000000 ) ) ;
#4933=CARTESIAN_POINT ( 'NONE',  ( 6.495190528383280260, 16.25000000000000000, 0.000000000000000000 ) ) ;
#4941=DIRECTION ( 'NONE',  ( 1.000000000000000000, 0.000000000000000000, 0.000000000000000000 ) ) ;
#4944=VERTEX_POINT ( 'NONE', #6145 ) ;
#4965=EDGE_LOOP ( 'NONE', ( #2258, #2361, #7386, #6412 ) ) ;
#4978=AXIS2_PLACEMENT_3D ( 'NONE', #5168, #7586, #4496 ) ;
#4979=ADVANCED_BREP_SHAPE_REPRESENTATION ( '', ( #1475, #5785 ), #1293 ) ;
#4995=CARTESIAN_POINT ( 'NONE',  ( -12.50000000000000000, 0.000000000000000000, 7.500000000000000000 ) ) ;
#5012=VERTEX_POINT ( 'NONE', #5459 ) ;
#5016=CARTESIAN_POINT ( 'NONE',  ( -9.381941874331412023, -16.24999999999999645, 7.500000000000000000 ) ) ;
#5043=ORIENTED_EDGE ( 'NONE', *, *, #504, .F. ) ;
#5060=VECTOR ( 'NONE', #2403, 1000.000000000000000 ) ;
#5071=EDGE_CURVE ( 'NONE', #3842, #1519, #92, .T. ) ;
#5079=ADVANCED_FACE ( 'NONE', ( #4563 ), #7524, .T. ) ;
#5086=DIRECTION ( 'NONE',  ( -0.000000000000000000, -0.000000000000000000, 1.000000000000000000 ) ) ;
#5089=ORIENTED_EDGE ( 'NONE', *, *, #3726, .F. ) ;
#5095=CARTESIAN_POINT ( 'NONE',  ( 0.000000000000000000, 0.000000000000000000, 6.999999999999999112 ) ) ;
#5142=VERTEX_POINT ( 'NONE', #2726 ) ;
#5144=VERTEX_POINT ( 'NONE', #121 ) ;
#5168=CARTESIAN_POINT ( 'NONE',  ( -12.99038105676657651, 1.734723475976807094E-15, 0.000000000000000000 ) ) ;
#5173=AXIS2_PLACEMENT_3D ( 'NONE', #7511, #6345, #3753 ) ;
#5206=ORIENTED_EDGE ( 'NONE', *, *, #6348, .F. ) ;
#5215=CIRCLE ( 'NONE', #503, 13.00000000000000178 ) ;
#5218=SHAPE_REPRESENTATION_RELATIONSHIP ( 'NONE' , 'NONE' ,  #7467, #4979 ) ;
#5228=AXIS2_PLACEMENT_3D ( 'NONE', #7072, #7757, #2266 ) ;
#5247=DIRECTION ( 'NONE',  ( -0.000000000000000000, 0.000000000000000000, -1.000000000000000000 ) ) ;
#5280=DIRECTION ( 'NONE',  ( 1.000000000000000000, 0.000000000000000000, 0.000000000000000000 ) ) ;
#5283=ORIENTED_EDGE ( 'NONE', *, *, #4634, .F. ) ;
#5303=SHAPE_DEFINITION_REPRESENTATION ( #6423, #7467 ) ;
#5315=EDGE_CURVE ( 'NONE', #3842, #2150, #5215, .T. ) ;
#5323=ADVANCED_FACE ( 'NONE', ( #4640 ), #3597, .T. ) ;
#5327=DIRECTION ( 'NONE',  ( -0.000000000000000000, -0.000000000000000000, 1.000000000000000000 ) ) ;
#5342=CARTESIAN_POINT ( 'NONE',  ( -6.495190528383282036, -11.24999999999999645, 0.000000000000000000 ) ) ;
#5350=CYLINDRICAL_SURFACE ( 'NONE', #2546, 5.000000000000000000 ) ;
#5351=CARTESIAN_POINT ( 'NONE',  ( 17.32050807568877104, 2.500000000000000888, 7.500000000000000000 ) ) ;
#5359=APPLICATION_CONTEXT ( 'automotive_design' ) ;
#5362=CYLINDRICAL_SURFACE ( 'NONE', #4521, 5.000000000000000000 ) ;
#5369=ORIENTED_EDGE ( 'NONE', *, *, #346, .T. ) ;
#5381=DIRECTION ( 'NONE',  ( 1.000000000000000000, 1.040834085586084257E-15, 0.000000000000000000 ) ) ;
#5385=CARTESIAN_POINT ( 'NONE',  ( -17.32050807568877104, -2.499999999999999112, 0.000000000000000000 ) ) ;
#5387=PRODUCT_CONTEXT ( 'NONE', #5359, 'mechanical' ) ;
#5395=ORIENTED_EDGE ( 'NONE', *, *, #2242, .T. ) ;
#5442=EDGE_LOOP ( 'NONE', ( #2067, #5842, #4488, #6527 ) ) ;
#5447=CIRCLE ( 'NONE', #7496, 5.000000000000000000 ) ;
#5450=VERTEX_POINT ( 'NONE', #2586 ) ;
#5455=CARTESIAN_POINT ( 'NONE',  ( 6.495190528383288253, -16.24999999999999645, 0.000000000000000000 ) ) ;
#5459=CARTESIAN_POINT ( 'NONE',  ( -17.32050807568877104, 2.500000000000002220, 0.000000000000000000 ) ) ;
#5467=CIRCLE ( 'NONE', #7004, 12.50000000000000000 ) ;
#5471=CARTESIAN_POINT ( 'NONE',  ( 6.495190528383289141, -11.24999999999999645, 0.000000000000000000 ) ) ;
#5474=AXIS2_PLACEMENT_3D ( 'NONE', #2944, #6624, #5381 ) ;
#5505=DIRECTION ( 'NONE',  ( 1.224646799147353207E-16, 1.000000000000000000, 0.000000000000000000 ) ) ;
#5506=VECTOR ( 'NONE', #5327, 1000.000000000000000 ) ;
#5511=DIRECTION ( 'NONE',  ( 0.000000000000000000, -0.000000000000000000, 1.000000000000000000 ) ) ;
#5523=AXIS2_PLACEMENT_3D ( 'NONE', #3396, #3989, #904 ) ;
#5532=CARTESIAN_POINT ( 'NONE',  ( 0.000000000000000000, 0.000000000000000000, 0.5000000000000004441 ) ) ;
#5539=CARTESIAN_POINT ( 'NONE',  ( -6.495190528383282036, -16.24999999999999645, 7.500000000000000000 ) ) ;
#5547=DIRECTION ( 'NONE',  ( -0.000000000000000000, 0.000000000000000000, -1.000000000000000000 ) ) ;
#5554=DIRECTION ( 'NONE',  ( 0.000000000000000000, -0.000000000000000000, 1.000000000000000000 ) ) ;
#5601=LINE ( 'NONE', #4995, #1075 ) ;
#5617=ORIENTED_EDGE ( 'NONE', *, *, #5315, .F. ) ;
#5636=CARTESIAN_POINT ( 'NONE',  ( 10.82531754730547213, 13.75000000000000178, 7.500000000000000000 ) ) ;
#5658=ORIENTED_EDGE ( 'NONE', *, *, #85, .F. ) ;
#5675=( NAMED_UNIT ( * ) PLANE_ANGLE_UNIT ( ) SI_UNIT ( $, .RADIAN. ) );
#5680=CYLINDRICAL_SURFACE ( 'NONE', #6209, 5.000000000000000888 ) ;
#5705=CIRCLE ( 'NONE', #5958, 12.50000000000000000 ) ;
#5731=ORIENTED_EDGE ( 'NONE', *, *, #4828, .T. ) ;
#5740=ADVANCED_FACE ( 'NONE', ( #7278 ), #5350, .T. ) ;
#5757=AXIS2_PLACEMENT_3D ( 'NONE', #3244, #1214, #1255 ) ;
#5762=DIRECTION ( 'NONE',  ( 0.000000000000000000, -0.000000000000000000, 1.000000000000000000 ) ) ;
#5777=DIRECTION ( 'NONE',  ( 0.000000000000000000, 0.000000000000000000, -1.000000000000000000 ) ) ;
#5780=DIRECTION ( 'NONE',  ( 1.224646799147353207E-16, 1.000000000000000000, 0.000000000000000000 ) ) ;
#5785=AXIS2_PLACEMENT_3D ( 'NONE', #4110, #4186, #2351 ) ;
#5819=EDGE_CURVE ( 'NONE', #1396, #268, #2271, .T. ) ;
#5831=AXIS2_PLACEMENT_3D ( 'NONE', #2089, #4536, #7510 ) ;
#5833=VERTEX_POINT ( 'NONE', #1097 ) ;
#5842=ORIENTED_EDGE ( 'NONE', *, *, #490, .T. ) ;
#5877=CIRCLE ( 'NONE', #4978, 5.000000000000000888 ) ;
#5899=CARTESIAN_POINT ( 'NONE',  ( 0.000000000000000000, 0.000000000000000000, 0.000000000000000000 ) ) ;
#5904=DIRECTION ( 'NONE',  ( 0.000000000000000000, 0.000000000000000000, -1.000000000000000000 ) ) ;
#5914=CARTESIAN_POINT ( 'NONE',  ( 0.000000000000000000, 0.000000000000000000, 0.5000000000000004441 ) ) ;
#5920=VERTEX_POINT ( 'NONE', #6828 ) ;
#5926=ORIENTED_EDGE ( 'NONE', *, *, #567, .T. ) ;
#5937=VECTOR ( 'NONE', #1560, 1000.000000000000000 ) ;
#5949=CIRCLE ( 'NONE', #1335, 5.000000000000000888 ) ;
#5955=LINE ( 'NONE', #5351, #2362 ) ;
#5958=AXIS2_PLACEMENT_3D ( 'NONE', #5532, #4281, #4922 ) ;
#5983=ADVANCED_FACE ( 'NONE', ( #2577 ), #732, .F. ) ;
#5988=DIRECTION ( 'NONE',  ( -1.000000000000000000, 1.224646799147353454E-16, 0.000000000000000000 ) ) ;
#6041=EDGE_CURVE ( 'NONE', #2004, #5012, #5877, .T. ) ;
#6053=ORIENTED_EDGE ( 'NONE', *, *, #4395, .F. ) ;
#6074=DIRECTION ( 'NONE',  ( -0.000000000000000000, 0.000000000000000000, -1.000000000000000000 ) ) ;
#6086=AXIS2_PLACEMENT_3D ( 'NONE', #5471, #6074, #4941 ) ;
#6094=ORIENTED_EDGE ( 'NONE', *, *, #7332, .F. ) ;
#6096=ORIENTED_EDGE ( 'NONE', *, *, #1374, .F. ) ;
#6112=CARTESIAN_POINT ( 'NONE',  ( -18.76388374866283471, 7.854341805648601650E-17, 7.500000000000000000 ) ) ;
#6133=EDGE_LOOP ( 'NONE', ( #6394, #1423, #7146, #6714 ) ) ;
#6138=ADVANCED_FACE ( 'NONE', ( #3256 ), #3576, .T. ) ;
#6143=ORIENTED_EDGE ( 'NONE', *, *, #7391, .T. ) ;
#6145=CARTESIAN_POINT ( 'NONE',  ( -13.00000000000000178, 1.592040838891559293E-15, 2.168404344971008868E-16 ) ) ;
#6164=PLANE ( 'NONE',  #1334 ) ;
#6193=LINE ( 'NONE', #1968, #449 ) ;
#6198=DIRECTION ( 'NONE',  ( 0.000000000000000000, -0.000000000000000000, 1.000000000000000000 ) ) ;
#6200=CARTESIAN_POINT ( 'NONE',  ( 10.82531754730548279, -13.74999999999999645, 7.500000000000000000 ) ) ;
#6201=CARTESIAN_POINT ( 'NONE',  ( 17.32050807568877104, -2.500000000000002220, 7.500000000000000000 ) ) ;
#6202=ORIENTED_EDGE ( 'NONE', *, *, #7618, .T. ) ;
#6209=AXIS2_PLACEMENT_3D ( 'NONE', #7519, #2629, #6959 ) ;
#6210=EDGE_LOOP ( 'NONE', ( #5089, #5206, #474, #4000 ) ) ;
#6211=AXIS2_PLACEMENT_3D ( 'NONE', #2578, #3673, #6231 ) ;
#6212=CARTESIAN_POINT ( 'NONE',  ( 17.32050807568877104, 2.500000000000000444, 7.500000000000000000 ) ) ;
#6220=VECTOR ( 'NONE', #1051, 1000.000000000000227 ) ;
#6231=DIRECTION ( 'NONE',  ( 1.000000000000000000, 0.000000000000000000, -0.000000000000000000 ) ) ;
#6247=CARTESIAN_POINT ( 'NONE',  ( 0.000000000000000000, 0.000000000000000000, 7.500000000000000000 ) ) ;
#6255=ORIENTED_EDGE ( 'NONE', *, *, #6670, .F. ) ;
#6274=CARTESIAN_POINT ( 'NONE',  ( 6.495190528383280260, 11.25000000000000000, 0.000000000000000000 ) ) ;
#6296=ORIENTED_EDGE ( 'NONE', *, *, #960, .F. ) ;
#6308=LINE ( 'NONE', #3112, #4794 ) ;
#6315=DIRECTION ( 'NONE',  ( 1.000000000000000000, 0.000000000000000000, 0.000000000000000000 ) ) ;
#6336=LINE ( 'NONE', #4605, #5937 ) ;
#6345=DIRECTION ( 'NONE',  ( 0.000000000000000000, -0.000000000000000000, 1.000000000000000000 ) ) ;
#6348=EDGE_CURVE ( 'NONE', #268, #3478, #118, .T. ) ;
#6350=DIRECTION ( 'NONE',  ( 1.000000000000000000, -1.734723475976807094E-15, 0.000000000000000000 ) ) ;
#6373=VERTEX_POINT ( 'NONE', #4933 ) ;
#6380=AXIS2_PLACEMENT_3D ( 'NONE', #6274, #171, #6350 ) ;
#6394=ORIENTED_EDGE ( 'NONE', *, *, #7091, .F. ) ;
#6397=DIRECTION ( 'NONE',  ( -0.000000000000000000, -0.000000000000000000, -1.000000000000000000 ) ) ;
#6399=CARTESIAN_POINT ( 'NONE',  ( 0.000000000000000000, 0.000000000000000000, 0.000000000000000000 ) ) ;
#6402=UNCERTAINTY_MEASURE_WITH_UNIT (LENGTH_MEASURE( 1.000000000000000082E-05 ), #2786, 'distance_accuracy_value', 'NONE');
#6412=ORIENTED_EDGE ( 'NONE', *, *, #1747, .F. ) ;
#6423=PRODUCT_DEFINITION_SHAPE ( 'NONE', 'NONE',  #2231 ) ;
#6425=FACE_OUTER_BOUND ( 'NONE', #699, .T. ) ;
#6429=LINE ( 'NONE', #6551, #6220 ) ;
#6431=VERTEX_POINT ( 'NONE', #612 ) ;
#6441=ORIENTED_EDGE ( 'NONE', *, *, #4331, .F. ) ;
#6450=VERTEX_POINT ( 'NONE', #5539 ) ;
#6462=MECHANICAL_DESIGN_GEOMETRIC_PRESENTATION_REPRESENTATION('',(#4283),#453);
#6474=DIRECTION ( 'NONE',  ( 0.000000000000000000, -0.000000000000000000, 1.000000000000000000 ) ) ;
#6492=EDGE_LOOP ( 'NONE', ( #789, #5395, #6813, #5283 ) ) ;
#6500=DIRECTION ( 'NONE',  ( 1.000000000000000000, 0.000000000000000000, -0.000000000000000000 ) ) ;
#6511=DIRECTION ( 'NONE',  ( 1.000000000000000000, 1.040834085586084257E-15, 0.000000000000000000 ) ) ;
#6517=DIRECTION ( 'NONE',  ( 0.5000000000000000000, 0.8660254037844385966, 0.000000000000000000 ) ) ;
#6527=ORIENTED_EDGE ( 'NONE', *, *, #760, .T. ) ;
#6531=EDGE_CURVE ( 'NONE', #3303, #603, #3335, .T. ) ;
#6539=ORIENTED_EDGE ( 'NONE', *, *, #5819, .T. ) ;
#6551=CARTESIAN_POINT ( 'NONE',  ( 9.381941874331417353, -16.24999999999999645, 7.500000000000000000 ) ) ;
#6573=ORIENTED_EDGE ( 'NONE', *, *, #525, .T. ) ;
#6574=DIRECTION ( 'NONE',  ( 1.000000000000000000, 0.000000000000000000, 0.000000000000000000 ) ) ;
#6605=EDGE_LOOP ( 'NONE', ( #1878, #300 ) ) ;
#6609=VERTEX_POINT ( 'NONE', #2167 ) ;
#6624=DIRECTION ( 'NONE',  ( -0.000000000000000000, 0.000000000000000000, -1.000000000000000000 ) ) ;
#6630=AXIS2_PLACEMENT_3D ( 'NONE', #1361, #2648, #7019 ) ;
#6653=EDGE_CURVE ( 'NONE', #4276, #1620, #2328, .T. ) ;
#6662=ORIENTED_EDGE ( 'NONE', *, *, #4235, .T. ) ;
#6670=EDGE_CURVE ( 'NONE', #109, #4276, #4071, .T. ) ;
#6694=CYLINDRICAL_SURFACE ( 'NONE', #963, 5.000000000000000888 ) ;
#6708=CLOSED_SHELL ( 'NONE', ( #6138, #5079, #4725, #3849, #687, #1441, #2243, #4185, #2389, #4243, #1492, #5983, #2474, #2749, #135, #5323, #1564, #5740, #303, #4342, #1933 ) ) ;
#6714=ORIENTED_EDGE ( 'NONE', *, *, #7535, .F. ) ;
#6724=EDGE_LOOP ( 'NONE', ( #3394, #1517 ) ) ;
#6726=ORIENTED_EDGE ( 'NONE', *, *, #7308, .T. ) ;
#6764=CARTESIAN_POINT ( 'NONE',  ( -17.32050807568877104, 2.500000000000002220, 7.500000000000000000 ) ) ;
#6811=EDGE_LOOP ( 'NONE', ( #5617, #4182, #737, #3600 ) ) ;
#6813=ORIENTED_EDGE ( 'NONE', *, *, #1728, .F. ) ;
#6825=DIRECTION ( 'NONE',  ( -1.000000000000000000, 0.000000000000000000, 0.000000000000000000 ) ) ;
#6828=CARTESIAN_POINT ( 'NONE',  ( -12.50000000000000000, 0.000000000000000000, 0.5000000000000004441 ) ) ;
#6831=ORIENTED_EDGE ( 'NONE', *, *, #4331, .T. ) ;
#6848=EDGE_CURVE ( 'NONE', #3797, #5144, #2719, .T. ) ;
#6876=ORIENTED_EDGE ( 'NONE', *, *, #3488, .T. ) ;
#6891=VERTEX_POINT ( 'NONE', #271 ) ;
#6903=ORIENTED_EDGE ( 'NONE', *, *, #364, .T. ) ;
#6909=CARTESIAN_POINT ( 'NONE',  ( 9.381941874331406694, 16.25000000000000000, 7.500000000000000000 ) ) ;
#6921=FACE_OUTER_BOUND ( 'NONE', #996, .T. ) ;
#6958=LINE ( 'NONE', #3310, #3134 ) ;
#6959=DIRECTION ( 'NONE',  ( -1.000000000000000000, 0.000000000000000000, 0.000000000000000000 ) ) ;
#6968=VECTOR ( 'NONE', #703, 1000.000000000000000 ) ;
#6972=ORIENTED_EDGE ( 'NONE', *, *, #787, .F. ) ;
#6989=DIRECTION ( 'NONE',  ( -0.000000000000000000, 0.000000000000000000, -1.000000000000000000 ) ) ;
#6995=DIRECTION ( 'NONE',  ( 0.000000000000000000, -0.000000000000000000, 1.000000000000000000 ) ) ;
#6997=DIRECTION ( 'NONE',  ( 1.000000000000000000, 0.000000000000000000, 0.000000000000000000 ) ) ;
#7004=AXIS2_PLACEMENT_3D ( 'NONE', #3793, #6198, #6315 ) ;
#7019=DIRECTION ( 'NONE',  ( 1.000000000000000000, 0.000000000000000000, 0.000000000000000000 ) ) ;
#7022=AXIS2_PLACEMENT_3D ( 'NONE', #1480, #5780, #1435 ) ;
#7064=ORIENTED_EDGE ( 'NONE', *, *, #7308, .F. ) ;
#7072=CARTESIAN_POINT ( 'NONE',  ( 13.00000000000000178, 0.000000000000000000, 6.999999999999999112 ) ) ;
#7091=EDGE_CURVE ( 'NONE', #5144, #5833, #4843, .T. ) ;
#7098=DIRECTION ( 'NONE',  ( -1.000000000000000000, 0.000000000000000000, 0.000000000000000000 ) ) ;
#7104=AXIS2_PLACEMENT_3D ( 'NONE', #632, #3157, #3086 ) ;
#7114=CIRCLE ( 'NONE', #1724, 13.00000000000000178 ) ;
#7115=EDGE_CURVE ( 'NONE', #6373, #5450, #2803, .T. ) ;
#7146=ORIENTED_EDGE ( 'NONE', *, *, #7115, .F. ) ;
#7156=VECTOR ( 'NONE', #3370, 1000.000000000000000 ) ;
#7161=AXIS2_PLACEMENT_3D ( 'NONE', #137, #6995, #1973 ) ;
#7163=DIRECTION ( 'NONE',  ( -0.5000000000000000000, -0.8660254037844385966, 0.000000000000000000 ) ) ;
#7195=CARTESIAN_POINT ( 'NONE',  ( -13.00000000000000178, 1.592040838891559293E-15, 0.5000000000000004441 ) ) ;
#7212=DIRECTION ( 'NONE',  ( 1.000000000000000000, 0.000000000000000000, 0.000000000000000000 ) ) ;
#7222=FACE_OUTER_BOUND ( 'NONE', #6210, .T. ) ;
#7223=ORIENTED_EDGE ( 'NONE', *, *, #776, .T. ) ;
#7240=EDGE_CURVE ( 'NONE', #6431, #4276, #3544, .T. ) ;
#7275=CARTESIAN_POINT ( 'NONE',  ( -9.381941874331415576, 16.25000000000000000, 0.000000000000000000 ) ) ;
#7278=FACE_OUTER_BOUND ( 'NONE', #6133, .T. ) ;
#7290=DIRECTION ( 'NONE',  ( 0.000000000000000000, -0.000000000000000000, 1.000000000000000000 ) ) ;
#7291=EDGE_CURVE ( 'NONE', #2150, #3303, #3828, .T. ) ;
#7292=EDGE_LOOP ( 'NONE', ( #867, #5369, #2274, #4305 ) ) ;
#7308=EDGE_CURVE ( 'NONE', #6609, #5012, #11, .T. ) ;
#7313=DIRECTION ( 'NONE',  ( -0.5000000000000000000, -0.8660254037844385966, 0.000000000000000000 ) ) ;
#7319=DIRECTION ( 'NONE',  ( 1.000000000000000000, 0.000000000000000000, 0.000000000000000000 ) ) ;
#7328=FACE_OUTER_BOUND ( 'NONE', #280, .T. ) ;
#7332=EDGE_CURVE ( 'NONE', #2517, #756, #618, .T. ) ;
#7338=ORIENTED_EDGE ( 'NONE', *, *, #3171, .F. ) ;
#7344=VERTEX_POINT ( 'NONE', #2420 ) ;
#7363=ORIENTED_EDGE ( 'NONE', *, *, #1311, .F. ) ;
#7386=ORIENTED_EDGE ( 'NONE', *, *, #7291, .T. ) ;
#7391=EDGE_CURVE ( 'NONE', #3478, #2517, #1274, .T. ) ;
#7395=VECTOR ( 'NONE', #7714, 1000.000000000000114 ) ;
#7408=DIRECTION ( 'NONE',  ( 1.000000000000000000, 0.000000000000000000, 0.000000000000000000 ) ) ;
#7425=ORIENTED_EDGE ( 'NONE', *, *, #1374, .T. ) ;
#7426=ORIENTED_EDGE ( 'NONE', *, *, #525, .F. ) ;
#7431=CARTESIAN_POINT ( 'NONE',  ( 0.000000000000000000, 0.000000000000000000, 7.500000000000000000 ) ) ;
#7438=CARTESIAN_POINT ( 'NONE',  ( -17.99038105676657651, 1.734723475976807094E-15, 0.000000000000000000 ) ) ;
#7453=ORIENTED_EDGE ( 'NONE', *, *, #490, .F. ) ;
#7456=CARTESIAN_POINT ( 'NONE',  ( 18.76388374866283471, -1.044563157018773529E-16, 7.500000000000000000 ) ) ;
#7467=SHAPE_REPRESENTATION ( 'Nut', ( #5785 ), #1293 ) ;
#7471=CARTESIAN_POINT ( 'NONE',  ( -10.82531754730547746, -13.74999999999999467, 7.500000000000000000 ) ) ;
#7474=TOROIDAL_SURFACE ( 'NONE', #5173, 13.00000000000000178, 0.5000000000000000000 ) ;
#7477=ORIENTED_EDGE ( 'NONE', *, *, #3171, .T. ) ;
#7489=AXIS2_PLACEMENT_3D ( 'NONE', #4267, #1230, #3683 ) ;
#7496=AXIS2_PLACEMENT_3D ( 'NONE', #5342, #4171, #6511 ) ;
#7506=DIRECTION ( 'NONE',  ( 0.000000000000000000, -0.000000000000000000, -1.000000000000000000 ) ) ;
#7510=DIRECTION ( 'NONE',  ( 1.000000000000000000, 0.000000000000000000, 0.000000000000000000 ) ) ;
#7511=CARTESIAN_POINT ( 'NONE',  ( 0.000000000000000000, 0.000000000000000000, 6.999999999999999112 ) ) ;
#7519=CARTESIAN_POINT ( 'NONE',  ( 12.99038105676657651, -1.301042606982605321E-15, 7.500000000000000000 ) ) ;
#7520=ORIENTED_EDGE ( 'NONE', *, *, #1932, .F. ) ;
#7521=CIRCLE ( 'NONE', #4437, 0.5000000000000000000 ) ;
#7524=TOROIDAL_SURFACE ( 'NONE', #6630, 13.00000000000000178, 0.5000000000000000000 ) ;
#7535=EDGE_CURVE ( 'NONE', #5833, #6373, #3364, .T. ) ;
#7536=ORIENTED_EDGE ( 'NONE', *, *, #85, .T. ) ;
#7540=VECTOR ( 'NONE', #7163, 1000.000000000000227 ) ;
#7550=DIRECTION ( 'NONE',  ( 0.000000000000000000, -0.000000000000000000, 1.000000000000000000 ) ) ;
#7552=DIRECTION ( 'NONE',  ( -1.000000000000000000, 0.000000000000000000, 0.000000000000000000 ) ) ;
#7561=CARTESIAN_POINT ( 'NONE',  ( -12.50000000000000000, 0.000000000000000000, 6.999999999999999112 ) ) ;
#7573=CARTESIAN_POINT ( 'NONE',  ( 6.495190528383280260, 16.25000000000000000, 7.500000000000000000 ) ) ;
#7585=CARTESIAN_POINT ( 'NONE',  ( -12.99038105676657651, 1.734723475976807094E-15, 7.500000000000000000 ) ) ;
#7586=DIRECTION ( 'NONE',  ( -0.000000000000000000, 0.000000000000000000, -1.000000000000000000 ) ) ;
#7599=PRODUCT_DEFINITION_CONTEXT ( 'detailed design', #549, 'design' ) ;
#7606=VECTOR ( 'NONE', #2831, 1000.000000000000000 ) ;
#7612=VECTOR ( 'NONE', #692, 1000.000000000000000 ) ;
#7618=EDGE_CURVE ( 'NONE', #5012, #268, #439, .T. ) ;
#7622=CARTESIAN_POINT ( 'NONE',  ( -10.82531754730547746, -13.74999999999999467, 0.000000000000000000 ) ) ;
#7632=LINE ( 'NONE', #2745, #7395 ) ;
#7641=ORIENTED_EDGE ( 'NONE', *, *, #5819, .F. ) ;
#7654=VECTOR ( 'NONE', #714, 1000.000000000000114 ) ;
#7671=EDGE_CURVE ( 'NONE', #1396, #6609, #2401, .T. ) ;
#7680=DIRECTION ( 'NONE',  ( 1.000000000000000000, 0.000000000000000000, 0.000000000000000000 ) ) ;
#7714=DIRECTION ( 'NONE',  ( -0.5000000000000003331, 0.8660254037844383745, 0.000000000000000000 ) ) ;
#7716=DIRECTION ( 'NONE',  ( 0.000000000000000000, 0.000000000000000000, -1.000000000000000000 ) ) ;
#7742=AXIS2_PLACEMENT_3D ( 'NONE', #7431, #1926, #6825 ) ;
#7746=ORIENTED_EDGE ( 'NONE', *, *, #6670, .T. ) ;
#7757=DIRECTION ( 'NONE',  ( 0.000000000000000000, -1.000000000000000000, -0.000000000000000000 ) ) ;
#7771=EDGE_LOOP ( 'NONE', ( #6296, #265, #181, #2018 ) ) ;
#7801=AXIS2_PLACEMENT_3D ( 'NONE', #5016, #2462, #4898 ) ;
#7803=CARTESIAN_POINT ( 'NONE',  ( 0.000000000000000000, 0.000000000000000000, 6.999999999999999112 ) ) ;
#7829=EDGE_CURVE ( 'NONE', #5920, #603, #3460, .T. ) ;
#7830=CARTESIAN_POINT ( 'NONE',  ( -18.76388374866283471, 7.854341805648601650E-17, 0.000000000000000000 ) ) ;
#7856=ORIENTED_EDGE ( 'NONE', *, *, #960, .T. ) ;
#7869=CARTESIAN_POINT ( 'NONE',  ( 9.381941874331406694, 16.25000000000000000, 0.000000000000000000 ) ) ;
#7878=DIRECTION ( 'NONE',  ( 0.000000000000000000, 0.000000000000000000, -1.000000000000000000 ) ) ;
#7880=FACE_BOUND ( 'NONE', #6724, .T. ) ;
#7899=CIRCLE ( 'NONE', #5474, 5.000000000000000000 ) ;
#7908=DIRECTION ( 'NONE',  ( 1.000000000000000000, 0.000000000000000000, 0.000000000000000000 ) ) ;
#7963=COLOUR_RGB('Black',0.12,0.14,0.17);
#7964=FILL_AREA_STYLE_COLOUR('',#7963);
#7965=FILL_AREA_STYLE('',(#7964));
#7966=SURFACE_STYLE_FILL_AREA(#7965);
#7967=SURFACE_SIDE_STYLE('',(#7966));
#7968=SURFACE_STYLE_USAGE(.BOTH.,#7967);
#7969=PRESENTATION_STYLE_ASSIGNMENT((#7968));
ENDSEC;
END-ISO-10303-21;
